ISO-10303-21;
HEADER;
/* Generated by software containing ST-Developer
 * from STEP Tools, Inc. (www.steptools.com) 
 */

FILE_DESCRIPTION(
/* description */ ('Compact handwheel screw vise'),
/* implementation_level */ '2;1');

FILE_NAME(
/* name */ 'Socket Set Screw - M5x8.step',
/* time_stamp */ '2026-10-29T16:08:22-07:00',
/* author */ (''),
/* organization */ (''),
/* preprocessor_version */ 'ST-DEVELOPER v20.2',
/* originating_system */ 'Autodesk Translation Framework v15.17.0.0',
/* authorisation */ '');

FILE_SCHEMA (('AUTOMOTIVE_DESIGN { 1 0 10303 214 3 1 1 }'));
ENDSEC;

DATA;
#10=MECHANICAL_DESIGN_GEOMETRIC_PRESENTATION_REPRESENTATION('',(#677),#25074);
#574=CONICAL_SURFACE('',#9129,0.235,0.785398163397448);
#575=CONICAL_SURFACE('',#9133,0.2125,0.785398163397448);
#613=SHAPE_REPRESENTATION_RELATIONSHIP('SRR','None',#25224,#641);
#641=ADVANCED_BREP_SHAPE_REPRESENTATION('',(#710),#25071);
#677=STYLED_ITEM('',(#25446),#710);
#710=MANIFOLD_SOLID_BREP('Body1',#8088);
#818=FACE_BOUND('',#2033,.T.);
#990=PLANE('',#9120);
#991=PLANE('',#9121);
#992=PLANE('',#9122);
#993=PLANE('',#9123);
#994=PLANE('',#9124);
#995=PLANE('',#9125);
#996=PLANE('',#9126);
#997=PLANE('',#9127);
#998=PLANE('',#9135);
#1449=FACE_OUTER_BOUND('',#2025,.T.);
#1450=FACE_OUTER_BOUND('',#2026,.T.);
#1451=FACE_OUTER_BOUND('',#2027,.T.);
#1452=FACE_OUTER_BOUND('',#2028,.T.);
#1453=FACE_OUTER_BOUND('',#2029,.T.);
#1454=FACE_OUTER_BOUND('',#2030,.T.);
#1455=FACE_OUTER_BOUND('',#2031,.T.);
#1456=FACE_OUTER_BOUND('',#2032,.T.);
#1457=FACE_OUTER_BOUND('',#2034,.T.);
#1458=FACE_OUTER_BOUND('',#2035,.T.);
#1459=FACE_OUTER_BOUND('',#2036,.T.);
#1460=FACE_OUTER_BOUND('',#2037,.T.);
#2025=EDGE_LOOP('',(#7219,#7220,#7221,#7222));
#2026=EDGE_LOOP('',(#7223,#7224,#7225,#7226));
#2027=EDGE_LOOP('',(#7227,#7228,#7229,#7230));
#2028=EDGE_LOOP('',(#7231,#7232,#7233,#7234));
#2029=EDGE_LOOP('',(#7235,#7236,#7237,#7238));
#2030=EDGE_LOOP('',(#7239,#7240,#7241,#7242));
#2031=EDGE_LOOP('',(#7243,#7244,#7245,#7246,#7247,#7248));
#2032=EDGE_LOOP('',(#7249));
#2033=EDGE_LOOP('',(#7250,#7251,#7252,#7253,#7254,#7255));
#2034=EDGE_LOOP('',(#7256,#7257,#7258,#7259));
#2035=EDGE_LOOP('',(#7260,#7261,#7262,#7263));
#2036=EDGE_LOOP('',(#7264,#7265,#7266,#7267));
#2037=EDGE_LOOP('',(#7268));
#2523=LINE('',#24839,#3031);
#2524=LINE('',#24841,#3032);
#2525=LINE('',#24843,#3033);
#2526=LINE('',#24844,#3034);
#2527=LINE('',#24847,#3035);
#2528=LINE('',#24849,#3036);
#2529=LINE('',#24850,#3037);
#2530=LINE('',#24853,#3038);
#2531=LINE('',#24855,#3039);
#2532=LINE('',#24856,#3040);
#2533=LINE('',#24859,#3041);
#2534=LINE('',#24861,#3042);
#2535=LINE('',#24862,#3043);
#2536=LINE('',#24865,#3044);
#2537=LINE('',#24867,#3045);
#2538=LINE('',#24868,#3046);
#2539=LINE('',#24870,#3047);
#2540=LINE('',#24871,#3048);
#2541=LINE('',#24879,#3049);
#2542=LINE('',#24883,#3050);
#2543=LINE('',#24887,#3051);
#3031=VECTOR('',#11105,1.);
#3032=VECTOR('',#11106,1.);
#3033=VECTOR('',#11107,1.);
#3034=VECTOR('',#11108,1.);
#3035=VECTOR('',#11111,1.);
#3036=VECTOR('',#11112,1.);
#3037=VECTOR('',#11113,1.);
#3038=VECTOR('',#11116,1.);
#3039=VECTOR('',#11117,1.);
#3040=VECTOR('',#11118,1.);
#3041=VECTOR('',#11121,1.);
#3042=VECTOR('',#11122,1.);
#3043=VECTOR('',#11123,1.);
#3044=VECTOR('',#11126,1.);
#3045=VECTOR('',#11127,1.);
#3046=VECTOR('',#11128,1.);
#3047=VECTOR('',#11131,1.);
#3048=VECTOR('',#11132,1.);
#3049=VECTOR('',#11143,0.235);
#3050=VECTOR('',#11148,0.25);
#3051=VECTOR('',#11153,0.2125);
#3317=CIRCLE('',#9128,0.22);
#3318=CIRCLE('',#9130,0.24505);
#3319=CIRCLE('',#9132,0.24505);
#3320=CIRCLE('',#9134,0.175);
#4026=VERTEX_POINT('',#24837);
#4027=VERTEX_POINT('',#24838);
#4028=VERTEX_POINT('',#24840);
#4029=VERTEX_POINT('',#24842);
#4030=VERTEX_POINT('',#24846);
#4031=VERTEX_POINT('',#24848);
#4032=VERTEX_POINT('',#24852);
#4033=VERTEX_POINT('',#24854);
#4034=VERTEX_POINT('',#24858);
#4035=VERTEX_POINT('',#24860);
#4036=VERTEX_POINT('',#24864);
#4037=VERTEX_POINT('',#24866);
#4038=VERTEX_POINT('',#24874);
#4039=VERTEX_POINT('',#24877);
#4040=VERTEX_POINT('',#24881);
#4041=VERTEX_POINT('',#24885);
#5096=EDGE_CURVE('',#4026,#4027,#2523,.T.);
#5097=EDGE_CURVE('',#4026,#4028,#2524,.T.);
#5098=EDGE_CURVE('',#4028,#4029,#2525,.T.);
#5099=EDGE_CURVE('',#4027,#4029,#2526,.T.);
#5100=EDGE_CURVE('',#4030,#4026,#2527,.T.);
#5101=EDGE_CURVE('',#4030,#4031,#2528,.T.);
#5102=EDGE_CURVE('',#4031,#4028,#2529,.T.);
#5103=EDGE_CURVE('',#4032,#4030,#2530,.T.);
#5104=EDGE_CURVE('',#4032,#4033,#2531,.T.);
#5105=EDGE_CURVE('',#4033,#4031,#2532,.T.);
#5106=EDGE_CURVE('',#4034,#4032,#2533,.T.);
#5107=EDGE_CURVE('',#4034,#4035,#2534,.T.);
#5108=EDGE_CURVE('',#4035,#4033,#2535,.T.);
#5109=EDGE_CURVE('',#4036,#4034,#2536,.T.);
#5110=EDGE_CURVE('',#4036,#4037,#2537,.T.);
#5111=EDGE_CURVE('',#4037,#4035,#2538,.T.);
#5112=EDGE_CURVE('',#4027,#4036,#2539,.T.);
#5113=EDGE_CURVE('',#4029,#4037,#2540,.T.);
#5114=EDGE_CURVE('',#4038,#4038,#3317,.T.);
#5115=EDGE_CURVE('',#4039,#4039,#3318,.T.);
#5116=EDGE_CURVE('',#4039,#4038,#2541,.T.);
#5117=EDGE_CURVE('',#4040,#4040,#3319,.F.);
#5118=EDGE_CURVE('',#4040,#4039,#2542,.T.);
#5119=EDGE_CURVE('',#4041,#4041,#3320,.T.);
#5120=EDGE_CURVE('',#4041,#4040,#2543,.T.);
#7219=ORIENTED_EDGE('',*,*,#5096,.F.);
#7220=ORIENTED_EDGE('',*,*,#5097,.T.);
#7221=ORIENTED_EDGE('',*,*,#5098,.T.);
#7222=ORIENTED_EDGE('',*,*,#5099,.F.);
#7223=ORIENTED_EDGE('',*,*,#5100,.F.);
#7224=ORIENTED_EDGE('',*,*,#5101,.T.);
#7225=ORIENTED_EDGE('',*,*,#5102,.T.);
#7226=ORIENTED_EDGE('',*,*,#5097,.F.);
#7227=ORIENTED_EDGE('',*,*,#5103,.F.);
#7228=ORIENTED_EDGE('',*,*,#5104,.T.);
#7229=ORIENTED_EDGE('',*,*,#5105,.T.);
#7230=ORIENTED_EDGE('',*,*,#5101,.F.);
#7231=ORIENTED_EDGE('',*,*,#5106,.F.);
#7232=ORIENTED_EDGE('',*,*,#5107,.T.);
#7233=ORIENTED_EDGE('',*,*,#5108,.T.);
#7234=ORIENTED_EDGE('',*,*,#5104,.F.);
#7235=ORIENTED_EDGE('',*,*,#5109,.F.);
#7236=ORIENTED_EDGE('',*,*,#5110,.T.);
#7237=ORIENTED_EDGE('',*,*,#5111,.T.);
#7238=ORIENTED_EDGE('',*,*,#5107,.F.);
#7239=ORIENTED_EDGE('',*,*,#5112,.F.);
#7240=ORIENTED_EDGE('',*,*,#5099,.T.);
#7241=ORIENTED_EDGE('',*,*,#5113,.T.);
#7242=ORIENTED_EDGE('',*,*,#5110,.F.);
#7243=ORIENTED_EDGE('',*,*,#5113,.F.);
#7244=ORIENTED_EDGE('',*,*,#5098,.F.);
#7245=ORIENTED_EDGE('',*,*,#5102,.F.);
#7246=ORIENTED_EDGE('',*,*,#5105,.F.);
#7247=ORIENTED_EDGE('',*,*,#5108,.F.);
#7248=ORIENTED_EDGE('',*,*,#5111,.F.);
#7249=ORIENTED_EDGE('',*,*,#5114,.F.);
#7250=ORIENTED_EDGE('',*,*,#5096,.T.);
#7251=ORIENTED_EDGE('',*,*,#5112,.T.);
#7252=ORIENTED_EDGE('',*,*,#5109,.T.);
#7253=ORIENTED_EDGE('',*,*,#5106,.T.);
#7254=ORIENTED_EDGE('',*,*,#5103,.T.);
#7255=ORIENTED_EDGE('',*,*,#5100,.T.);
#7256=ORIENTED_EDGE('',*,*,#5115,.F.);
#7257=ORIENTED_EDGE('',*,*,#5116,.T.);
#7258=ORIENTED_EDGE('',*,*,#5114,.T.);
#7259=ORIENTED_EDGE('',*,*,#5116,.F.);
#7260=ORIENTED_EDGE('',*,*,#5117,.F.);
#7261=ORIENTED_EDGE('',*,*,#5118,.T.);
#7262=ORIENTED_EDGE('',*,*,#5115,.T.);
#7263=ORIENTED_EDGE('',*,*,#5118,.F.);
#7264=ORIENTED_EDGE('',*,*,#5119,.F.);
#7265=ORIENTED_EDGE('',*,*,#5120,.T.);
#7266=ORIENTED_EDGE('',*,*,#5117,.T.);
#7267=ORIENTED_EDGE('',*,*,#5120,.F.);
#7268=ORIENTED_EDGE('',*,*,#5119,.T.);
#7577=CYLINDRICAL_SURFACE('',#9131,0.24505);
#8019=ADVANCED_FACE('',(#1449),#990,.F.);
#8020=ADVANCED_FACE('',(#1450),#991,.F.);
#8021=ADVANCED_FACE('',(#1451),#992,.F.);
#8022=ADVANCED_FACE('',(#1452),#993,.F.);
#8023=ADVANCED_FACE('',(#1453),#994,.F.);
#8024=ADVANCED_FACE('',(#1454),#995,.F.);
#8025=ADVANCED_FACE('',(#1455),#996,.F.);
#8026=ADVANCED_FACE('',(#1456,#818),#997,.T.);
#8027=ADVANCED_FACE('',(#1457),#574,.T.);
#8028=ADVANCED_FACE('',(#1458),#7577,.T.);
#8029=ADVANCED_FACE('',(#1459),#575,.T.);
#8030=ADVANCED_FACE('',(#1460),#998,.T.);
#8088=CLOSED_SHELL('',(#8019,#8020,#8021,#8022,#8023,#8024,#8025,#8026,
#8027,#8028,#8029,#8030));
#9119=AXIS2_PLACEMENT_3D('',#24835,#11101,#11102);
#9120=AXIS2_PLACEMENT_3D('',#24836,#11103,#11104);
#9121=AXIS2_PLACEMENT_3D('',#24845,#11109,#11110);
#9122=AXIS2_PLACEMENT_3D('',#24851,#11114,#11115);
#9123=AXIS2_PLACEMENT_3D('',#24857,#11119,#11120);
#9124=AXIS2_PLACEMENT_3D('',#24863,#11124,#11125);
#9125=AXIS2_PLACEMENT_3D('',#24869,#11129,#11130);
#9126=AXIS2_PLACEMENT_3D('',#24872,#11133,#11134);
#9127=AXIS2_PLACEMENT_3D('',#24873,#11135,#11136);
#9128=AXIS2_PLACEMENT_3D('',#24875,#11137,#11138);
#9129=AXIS2_PLACEMENT_3D('',#24876,#11139,#11140);
#9130=AXIS2_PLACEMENT_3D('',#24878,#11141,#11142);
#9131=AXIS2_PLACEMENT_3D('',#24880,#11144,#11145);
#9132=AXIS2_PLACEMENT_3D('',#24882,#11146,#11147);
#9133=AXIS2_PLACEMENT_3D('',#24884,#11149,#11150);
#9134=AXIS2_PLACEMENT_3D('',#24886,#11151,#11152);
#9135=AXIS2_PLACEMENT_3D('',#24888,#11154,#11155);
#11101=DIRECTION('axis',(0.,0.,1.));
#11102=DIRECTION('refdir',(1.,0.,0.));
#11103=DIRECTION('center_axis',(0.866025403784439,0.,-0.5));
#11104=DIRECTION('ref_axis',(0.5,0.,0.866025403784439));
#11105=DIRECTION('',(0.5,0.,0.866025403784439));
#11106=DIRECTION('',(0.,-1.,0.));
#11107=DIRECTION('',(0.5,0.,0.866025403784439));
#11108=DIRECTION('',(0.,-1.,0.));
#11109=DIRECTION('center_axis',(1.92296268638356E-16,0.,-1.));
#11110=DIRECTION('ref_axis',(1.,0.,1.92296268638356E-16));
#11111=DIRECTION('',(1.,0.,1.92296268638356E-16));
#11112=DIRECTION('',(0.,-1.,0.));
#11113=DIRECTION('',(1.,0.,1.92296268638356E-16));
#11114=DIRECTION('center_axis',(-0.866025403784439,0.,-0.5));
#11115=DIRECTION('ref_axis',(0.5,0.,-0.866025403784439));
#11116=DIRECTION('',(0.5,0.,-0.866025403784439));
#11117=DIRECTION('',(0.,-1.,0.));
#11118=DIRECTION('',(0.5,0.,-0.866025403784438));
#11119=DIRECTION('center_axis',(-0.866025403784439,0.,0.5));
#11120=DIRECTION('ref_axis',(-0.5,0.,-0.866025403784439));
#11121=DIRECTION('',(-0.5,0.,-0.866025403784439));
#11122=DIRECTION('',(0.,-1.,0.));
#11123=DIRECTION('',(-0.5,0.,-0.866025403784439));
#11124=DIRECTION('center_axis',(-1.92296268638356E-16,0.,1.));
#11125=DIRECTION('ref_axis',(-1.,0.,-1.92296268638356E-16));
#11126=DIRECTION('',(-1.,0.,-1.92296268638356E-16));
#11127=DIRECTION('',(0.,-1.,0.));
#11128=DIRECTION('',(-1.,0.,-1.92296268638356E-16));
#11129=DIRECTION('center_axis',(0.866025403784439,0.,0.5));
#11130=DIRECTION('ref_axis',(-0.5,0.,0.866025403784439));
#11131=DIRECTION('',(-0.5,0.,0.866025403784439));
#11132=DIRECTION('',(-0.5,0.,0.866025403784439));
#11133=DIRECTION('center_axis',(0.,-1.,0.));
#11134=DIRECTION('ref_axis',(0.,0.,-1.));
#11135=DIRECTION('center_axis',(0.,1.,0.));
#11136=DIRECTION('ref_axis',(0.,0.,1.));
#11137=DIRECTION('center_axis',(0.,-1.,0.));
#11138=DIRECTION('ref_axis',(1.,0.,0.));
#11139=DIRECTION('center_axis',(0.,-1.,0.));
#11140=DIRECTION('ref_axis',(1.,0.,0.));
#11141=DIRECTION('center_axis',(0.,-1.,0.));
#11142=DIRECTION('ref_axis',(1.,0.,0.));
#11143=DIRECTION('',(0.707106781186547,0.707106781186548,8.65956056235493E-17));
#11144=DIRECTION('center_axis',(0.,-1.,0.));
#11145=DIRECTION('ref_axis',(1.,0.,0.));
#11146=DIRECTION('center_axis',(0.,1.,0.));
#11147=DIRECTION('ref_axis',(1.,0.,0.));
#11148=DIRECTION('',(0.,1.,0.));
#11149=DIRECTION('center_axis',(0.,1.,0.));
#11150=DIRECTION('ref_axis',(1.,0.,0.));
#11151=DIRECTION('center_axis',(0.,-1.,0.));
#11152=DIRECTION('ref_axis',(1.,0.,0.));
#11153=DIRECTION('',(-0.707106781186547,0.707106781186548,-8.65956056235493E-17));
#11154=DIRECTION('center_axis',(0.,-1.,0.));
#11155=DIRECTION('ref_axis',(0.,0.,-1.));
#24835=CARTESIAN_POINT('',(0.,0.,0.));
#24836=CARTESIAN_POINT('Origin',(0.0721687836487032,0.,-0.125));
#24837=CARTESIAN_POINT('',(0.0721687836487032,0.,-0.125));
#24838=CARTESIAN_POINT('',(0.144337567297406,0.,0.));
#24839=CARTESIAN_POINT('',(0.117710979560879,0.,-0.0461186027918559));
#24840=CARTESIAN_POINT('',(0.0721687836487032,-0.25,-0.125));
#24841=CARTESIAN_POINT('',(0.0721687836487032,0.,-0.125));
#24842=CARTESIAN_POINT('',(0.144337567297406,-0.25,0.));
#24843=CARTESIAN_POINT('',(0.144337567297406,-0.25,0.));
#24844=CARTESIAN_POINT('',(0.144337567297406,0.,0.));
#24845=CARTESIAN_POINT('Origin',(-0.0721687836487032,0.,-0.125));
#24846=CARTESIAN_POINT('',(-0.0721687836487032,0.,-0.125));
#24847=CARTESIAN_POINT('',(0.0739156081756484,0.,-0.125));
#24848=CARTESIAN_POINT('',(-0.0721687836487032,-0.25,-0.125));
#24849=CARTESIAN_POINT('',(-0.0721687836487032,0.,-0.125));
#24850=CARTESIAN_POINT('',(0.0721687836487032,-0.25,-0.125));
#24851=CARTESIAN_POINT('Origin',(-0.144337567297406,0.,-4.16333634234434E-17));
#24852=CARTESIAN_POINT('',(-0.144337567297406,0.,-1.76762539787485E-17));
#24853=CARTESIAN_POINT('',(-0.0987953713852306,0.,-0.0788813972081442));
#24854=CARTESIAN_POINT('',(-0.144337567297406,-0.25,-2.77555756156289E-17));
#24855=CARTESIAN_POINT('',(-0.144337567297406,0.,-1.76762539787485E-17));
#24856=CARTESIAN_POINT('',(-0.0721687836487032,-0.25,-0.125));
#24857=CARTESIAN_POINT('Origin',(-0.0721687836487033,0.,0.125));
#24858=CARTESIAN_POINT('',(-0.0721687836487033,0.,0.125));
#24859=CARTESIAN_POINT('',(-0.0627109795608791,0.,0.141381397208144));
#24860=CARTESIAN_POINT('',(-0.0721687836487033,-0.25,0.125));
#24861=CARTESIAN_POINT('',(-0.0721687836487033,0.,0.125));
#24862=CARTESIAN_POINT('',(-0.144337567297406,-0.25,-1.76762539787485E-17));
#24863=CARTESIAN_POINT('Origin',(0.0721687836487032,0.,0.125));
#24864=CARTESIAN_POINT('',(0.0721687836487032,0.,0.125));
#24865=CARTESIAN_POINT('',(0.146084391824352,0.,0.125));
#24866=CARTESIAN_POINT('',(0.0721687836487032,-0.25,0.125));
#24867=CARTESIAN_POINT('',(0.0721687836487032,0.,0.125));
#24868=CARTESIAN_POINT('',(-0.0721687836487033,-0.25,0.125));
#24869=CARTESIAN_POINT('Origin',(0.144337567297406,0.,0.));
#24870=CARTESIAN_POINT('',(0.153795371385231,0.,-0.0163813972081441));
#24871=CARTESIAN_POINT('',(0.0721687836487032,-0.25,0.125));
#24872=CARTESIAN_POINT('Origin',(0.,-0.25,0.));
#24873=CARTESIAN_POINT('Origin',(0.22,0.,0.));
#24874=CARTESIAN_POINT('',(-0.22,-8.67361737988404E-18,-2.69422295812418E-17));
#24875=CARTESIAN_POINT('Origin',(0.,0.,0.));
#24876=CARTESIAN_POINT('Origin',(0.,-0.015,0.));
#24877=CARTESIAN_POINT('',(-0.24505,-0.02505,-3.00099698131059E-17));
#24878=CARTESIAN_POINT('Origin',(0.,-0.02505,0.));
#24879=CARTESIAN_POINT('',(-0.235,-0.015,-2.87791997799628E-17));
#24880=CARTESIAN_POINT('Origin',(0.,-0.3775,0.));
#24881=CARTESIAN_POINT('',(-0.24505,-0.72995,3.00099698131059E-17));
#24882=CARTESIAN_POINT('Origin',(0.,-0.72995,0.));
#24883=CARTESIAN_POINT('',(-0.24505,-0.3775,-3.00099698131059E-17));
#24884=CARTESIAN_POINT('Origin',(0.,-0.7625,0.));
#24885=CARTESIAN_POINT('',(-0.175,-0.8,-2.14313189850787E-17));
#24886=CARTESIAN_POINT('Origin',(0.,-0.8,0.));
#24887=CARTESIAN_POINT('',(-0.2125,-0.7625,-2.60237444818813E-17));
#24888=CARTESIAN_POINT('Origin',(0.,-0.8,0.));
#25037=UNCERTAINTY_MEASURE_WITH_UNIT(LENGTH_MEASURE(0.001),#25075,
'DISTANCE_ACCURACY_VALUE',
'Maximum model space distance between geometric entities at asserted c
onnectivities');
#25040=UNCERTAINTY_MEASURE_WITH_UNIT(LENGTH_MEASURE(0.001),#25075,
'DISTANCE_ACCURACY_VALUE',
'Maximum model space distance between geometric entities at asserted c
onnectivities');
#25071=(
GEOMETRIC_REPRESENTATION_CONTEXT(3)
GLOBAL_UNCERTAINTY_ASSIGNED_CONTEXT((#25037))
GLOBAL_UNIT_ASSIGNED_CONTEXT((#25075,#25077,#25078))
REPRESENTATION_CONTEXT('','3D')
);
#25074=(
GEOMETRIC_REPRESENTATION_CONTEXT(3)
GLOBAL_UNCERTAINTY_ASSIGNED_CONTEXT((#25040))
GLOBAL_UNIT_ASSIGNED_CONTEXT((#25075,#25077,#25078))
REPRESENTATION_CONTEXT('','3D')
);
#25075=(
LENGTH_UNIT()
NAMED_UNIT(*)
SI_UNIT(.CENTI.,.METRE.)
);
#25077=(
NAMED_UNIT(*)
PLANE_ANGLE_UNIT()
SI_UNIT($,.RADIAN.)
);
#25078=(
NAMED_UNIT(*)
SI_UNIT($,.STERADIAN.)
SOLID_ANGLE_UNIT()
);
#25109=SHAPE_DEFINITION_REPRESENTATION(#25158,#25224);
#25158=PRODUCT_DEFINITION_SHAPE('',$,#25258);
#25224=SHAPE_REPRESENTATION('',(#9119),#25071);
#25227=PRODUCT_DEFINITION_CONTEXT('part definition',#25328,'design');
#25258=PRODUCT_DEFINITION('Socket Set Screw - M5x8',
'Socket Set Screw - M5x8',#25291,#25227);
#25291=PRODUCT_DEFINITION_FORMATION('',$,#25360);
#25328=APPLICATION_CONTEXT(
'Core Data for Automotive Mechanical Design Process');
#25329=PRODUCT_CONTEXT('part definition',#25328,'mechanical');
#25360=PRODUCT('Socket Set Screw - M5x8','Socket Set Screw - M5x8',
'Socket Set Screw - M5x8',(#25329));
#25440=COLOUR_RGB('Black',0.12,0.14,0.17);
#25441=FILL_AREA_STYLE_COLOUR('',#25440);
#25442=FILL_AREA_STYLE('',(#25441));
#25443=SURFACE_STYLE_FILL_AREA(#25442);
#25444=SURFACE_SIDE_STYLE('',(#25443));
#25445=SURFACE_STYLE_USAGE(.BOTH.,#25444);
#25446=PRESENTATION_STYLE_ASSIGNMENT((#25445));
ENDSEC;
END-ISO-10303-21;
